ISO-10303-21;
HEADER;
/* Generated by software containing ST-Developer
 * from STEP Tools, Inc. (www.steptools.com) 
 */

FILE_DESCRIPTION(
/* description */ ('Ball-type isolation valve (generic)'),
/* implementation_level */ '2;1');

FILE_NAME(
/* name */ 'Cap Screw - M4x16.step',
/* time_stamp */ '2026-10-27T10:53:05-07:00',
/* author */ (''),
/* organization */ (''),
/* preprocessor_version */ 'ST-DEVELOPER v20.2',
/* originating_system */ 'Autodesk Translation Framework v15.17.0.0',
/* authorisation */ '');

FILE_SCHEMA (('AUTOMOTIVE_DESIGN { 1 0 10303 214 3 1 1 }'));
ENDSEC;

DATA;
#10=MECHANICAL_DESIGN_GEOMETRIC_PRESENTATION_REPRESENTATION('',(#296),#7425);
#211=CONICAL_SURFACE('',#4725,0.325,0.785398163397448);
#212=CONICAL_SURFACE('',#4729,0.335,0.785398163397448);
#213=CONICAL_SURFACE('',#4733,0.21,0.463647609000806);
#214=CONICAL_SURFACE('',#4737,0.18,0.785398163397448);
#219=ORIENTED_CLOSED_SHELL('',*,#4103,.F.);
#222=BREP_WITH_VOIDS('Body1',#4102,(#219));
#244=SHAPE_REPRESENTATION_RELATIONSHIP('SRR','None',#7554,#270);
#270=ADVANCED_BREP_SHAPE_REPRESENTATION('',(#222),#7417);
#296=STYLED_ITEM('',(#7751),#222);
#409=FACE_BOUND('',#1078,.T.);
#514=PLANE('',#4723);
#515=PLANE('',#4731);
#516=PLANE('',#4739);
#517=PLANE('',#4740);
#518=PLANE('',#4741);
#519=PLANE('',#4742);
#520=PLANE('',#4743);
#521=PLANE('',#4744);
#522=PLANE('',#4745);
#523=PLANE('',#4746);
#524=PLANE('',#4747);
#746=FACE_OUTER_BOUND('',#1073,.T.);
#747=FACE_OUTER_BOUND('',#1074,.T.);
#748=FACE_OUTER_BOUND('',#1075,.T.);
#749=FACE_OUTER_BOUND('',#1076,.T.);
#750=FACE_OUTER_BOUND('',#1077,.T.);
#751=FACE_OUTER_BOUND('',#1079,.T.);
#752=FACE_OUTER_BOUND('',#1080,.T.);
#753=FACE_OUTER_BOUND('',#1081,.T.);
#754=FACE_OUTER_BOUND('',#1082,.T.);
#755=FACE_OUTER_BOUND('',#1083,.T.);
#756=FACE_OUTER_BOUND('',#1084,.T.);
#757=FACE_OUTER_BOUND('',#1085,.T.);
#758=FACE_OUTER_BOUND('',#1086,.T.);
#759=FACE_OUTER_BOUND('',#1087,.T.);
#760=FACE_OUTER_BOUND('',#1088,.T.);
#761=FACE_OUTER_BOUND('',#1089,.T.);
#762=FACE_OUTER_BOUND('',#1090,.T.);
#1073=EDGE_LOOP('',(#3431));
#1074=EDGE_LOOP('',(#3432,#3433,#3434,#3435));
#1075=EDGE_LOOP('',(#3436,#3437,#3438,#3439));
#1076=EDGE_LOOP('',(#3440,#3441,#3442,#3443));
#1077=EDGE_LOOP('',(#3444));
#1078=EDGE_LOOP('',(#3445));
#1079=EDGE_LOOP('',(#3446,#3447,#3448,#3449));
#1080=EDGE_LOOP('',(#3450,#3451,#3452,#3453));
#1081=EDGE_LOOP('',(#3454,#3455,#3456,#3457));
#1082=EDGE_LOOP('',(#3458));
#1083=EDGE_LOOP('',(#3459,#3460,#3461,#3462));
#1084=EDGE_LOOP('',(#3463,#3464,#3465,#3466));
#1085=EDGE_LOOP('',(#3467,#3468,#3469,#3470));
#1086=EDGE_LOOP('',(#3471,#3472,#3473,#3474));
#1087=EDGE_LOOP('',(#3475,#3476,#3477,#3478));
#1088=EDGE_LOOP('',(#3479,#3480,#3481,#3482));
#1089=EDGE_LOOP('',(#3483,#3484,#3485,#3486,#3487,#3488));
#1090=EDGE_LOOP('',(#3489,#3490,#3491,#3492,#3493,#3494));
#1345=LINE('',#6964,#1653);
#1346=LINE('',#6968,#1654);
#1347=LINE('',#6972,#1655);
#1348=LINE('',#6979,#1656);
#1349=LINE('',#6983,#1657);
#1350=LINE('',#6987,#1658);
#1351=LINE('',#6992,#1659);
#1352=LINE('',#6994,#1660);
#1353=LINE('',#6996,#1661);
#1354=LINE('',#6997,#1662);
#1355=LINE('',#7000,#1663);
#1356=LINE('',#7002,#1664);
#1357=LINE('',#7003,#1665);
#1358=LINE('',#7006,#1666);
#1359=LINE('',#7008,#1667);
#1360=LINE('',#7009,#1668);
#1361=LINE('',#7012,#1669);
#1362=LINE('',#7014,#1670);
#1363=LINE('',#7015,#1671);
#1364=LINE('',#7018,#1672);
#1365=LINE('',#7020,#1673);
#1366=LINE('',#7021,#1674);
#1367=LINE('',#7023,#1675);
#1368=LINE('',#7024,#1676);
#1653=VECTOR('',#5734,0.325);
#1654=VECTOR('',#5739,0.35);
#1655=VECTOR('',#5744,0.335);
#1656=VECTOR('',#5753,0.21);
#1657=VECTOR('',#5758,0.2);
#1658=VECTOR('',#5763,0.18);
#1659=VECTOR('',#5768,1.);
#1660=VECTOR('',#5769,1.);
#1661=VECTOR('',#5770,1.);
#1662=VECTOR('',#5771,1.);
#1663=VECTOR('',#5774,1.);
#1664=VECTOR('',#5775,1.);
#1665=VECTOR('',#5776,1.);
#1666=VECTOR('',#5779,1.);
#1667=VECTOR('',#5780,1.);
#1668=VECTOR('',#5781,1.);
#1669=VECTOR('',#5784,1.);
#1670=VECTOR('',#5785,1.);
#1671=VECTOR('',#5786,1.);
#1672=VECTOR('',#5789,1.);
#1673=VECTOR('',#5790,1.);
#1674=VECTOR('',#5791,1.);
#1675=VECTOR('',#5794,1.);
#1676=VECTOR('',#5795,1.);
#1917=CIRCLE('',#4724,0.3);
#1918=CIRCLE('',#4726,0.35);
#1919=CIRCLE('',#4728,0.35);
#1920=CIRCLE('',#4730,0.32);
#1921=CIRCLE('',#4732,0.22);
#1922=CIRCLE('',#4734,0.1954);
#1923=CIRCLE('',#4736,0.1954);
#1924=CIRCLE('',#4738,0.16);
#2173=VERTEX_POINT('',#6959);
#2174=VERTEX_POINT('',#6962);
#2175=VERTEX_POINT('',#6966);
#2176=VERTEX_POINT('',#6970);
#2177=VERTEX_POINT('',#6974);
#2178=VERTEX_POINT('',#6977);
#2179=VERTEX_POINT('',#6981);
#2180=VERTEX_POINT('',#6985);
#2181=VERTEX_POINT('',#6990);
#2182=VERTEX_POINT('',#6991);
#2183=VERTEX_POINT('',#6993);
#2184=VERTEX_POINT('',#6995);
#2185=VERTEX_POINT('',#6999);
#2186=VERTEX_POINT('',#7001);
#2187=VERTEX_POINT('',#7005);
#2188=VERTEX_POINT('',#7007);
#2189=VERTEX_POINT('',#7011);
#2190=VERTEX_POINT('',#7013);
#2191=VERTEX_POINT('',#7017);
#2192=VERTEX_POINT('',#7019);
#2608=EDGE_CURVE('',#2173,#2173,#1917,.T.);
#2609=EDGE_CURVE('',#2174,#2174,#1918,.T.);
#2610=EDGE_CURVE('',#2174,#2173,#1345,.T.);
#2611=EDGE_CURVE('',#2175,#2175,#1919,.T.);
#2612=EDGE_CURVE('',#2175,#2174,#1346,.T.);
#2613=EDGE_CURVE('',#2176,#2176,#1920,.T.);
#2614=EDGE_CURVE('',#2176,#2175,#1347,.T.);
#2615=EDGE_CURVE('',#2177,#2177,#1921,.T.);
#2616=EDGE_CURVE('',#2178,#2178,#1922,.F.);
#2617=EDGE_CURVE('',#2178,#2177,#1348,.T.);
#2618=EDGE_CURVE('',#2179,#2179,#1923,.F.);
#2619=EDGE_CURVE('',#2179,#2178,#1349,.T.);
#2620=EDGE_CURVE('',#2180,#2180,#1924,.T.);
#2621=EDGE_CURVE('',#2180,#2179,#1350,.T.);
#2622=EDGE_CURVE('',#2181,#2182,#1351,.T.);
#2623=EDGE_CURVE('',#2182,#2183,#1352,.T.);
#2624=EDGE_CURVE('',#2183,#2184,#1353,.T.);
#2625=EDGE_CURVE('',#2181,#2184,#1354,.T.);
#2626=EDGE_CURVE('',#2182,#2185,#1355,.T.);
#2627=EDGE_CURVE('',#2185,#2186,#1356,.T.);
#2628=EDGE_CURVE('',#2186,#2183,#1357,.T.);
#2629=EDGE_CURVE('',#2185,#2187,#1358,.T.);
#2630=EDGE_CURVE('',#2187,#2188,#1359,.T.);
#2631=EDGE_CURVE('',#2188,#2186,#1360,.T.);
#2632=EDGE_CURVE('',#2187,#2189,#1361,.T.);
#2633=EDGE_CURVE('',#2189,#2190,#1362,.T.);
#2634=EDGE_CURVE('',#2190,#2188,#1363,.T.);
#2635=EDGE_CURVE('',#2189,#2191,#1364,.T.);
#2636=EDGE_CURVE('',#2191,#2192,#1365,.T.);
#2637=EDGE_CURVE('',#2192,#2190,#1366,.T.);
#2638=EDGE_CURVE('',#2191,#2181,#1367,.T.);
#2639=EDGE_CURVE('',#2184,#2192,#1368,.T.);
#3431=ORIENTED_EDGE('',*,*,#2608,.F.);
#3432=ORIENTED_EDGE('',*,*,#2609,.F.);
#3433=ORIENTED_EDGE('',*,*,#2610,.T.);
#3434=ORIENTED_EDGE('',*,*,#2608,.T.);
#3435=ORIENTED_EDGE('',*,*,#2610,.F.);
#3436=ORIENTED_EDGE('',*,*,#2611,.F.);
#3437=ORIENTED_EDGE('',*,*,#2612,.T.);
#3438=ORIENTED_EDGE('',*,*,#2609,.T.);
#3439=ORIENTED_EDGE('',*,*,#2612,.F.);
#3440=ORIENTED_EDGE('',*,*,#2613,.F.);
#3441=ORIENTED_EDGE('',*,*,#2614,.T.);
#3442=ORIENTED_EDGE('',*,*,#2611,.T.);
#3443=ORIENTED_EDGE('',*,*,#2614,.F.);
#3444=ORIENTED_EDGE('',*,*,#2613,.T.);
#3445=ORIENTED_EDGE('',*,*,#2615,.F.);
#3446=ORIENTED_EDGE('',*,*,#2616,.F.);
#3447=ORIENTED_EDGE('',*,*,#2617,.T.);
#3448=ORIENTED_EDGE('',*,*,#2615,.T.);
#3449=ORIENTED_EDGE('',*,*,#2617,.F.);
#3450=ORIENTED_EDGE('',*,*,#2618,.F.);
#3451=ORIENTED_EDGE('',*,*,#2619,.T.);
#3452=ORIENTED_EDGE('',*,*,#2616,.T.);
#3453=ORIENTED_EDGE('',*,*,#2619,.F.);
#3454=ORIENTED_EDGE('',*,*,#2620,.F.);
#3455=ORIENTED_EDGE('',*,*,#2621,.T.);
#3456=ORIENTED_EDGE('',*,*,#2618,.T.);
#3457=ORIENTED_EDGE('',*,*,#2621,.F.);
#3458=ORIENTED_EDGE('',*,*,#2620,.T.);
#3459=ORIENTED_EDGE('',*,*,#2622,.T.);
#3460=ORIENTED_EDGE('',*,*,#2623,.T.);
#3461=ORIENTED_EDGE('',*,*,#2624,.T.);
#3462=ORIENTED_EDGE('',*,*,#2625,.F.);
#3463=ORIENTED_EDGE('',*,*,#2626,.T.);
#3464=ORIENTED_EDGE('',*,*,#2627,.T.);
#3465=ORIENTED_EDGE('',*,*,#2628,.T.);
#3466=ORIENTED_EDGE('',*,*,#2623,.F.);
#3467=ORIENTED_EDGE('',*,*,#2629,.T.);
#3468=ORIENTED_EDGE('',*,*,#2630,.T.);
#3469=ORIENTED_EDGE('',*,*,#2631,.T.);
#3470=ORIENTED_EDGE('',*,*,#2627,.F.);
#3471=ORIENTED_EDGE('',*,*,#2632,.T.);
#3472=ORIENTED_EDGE('',*,*,#2633,.T.);
#3473=ORIENTED_EDGE('',*,*,#2634,.T.);
#3474=ORIENTED_EDGE('',*,*,#2630,.F.);
#3475=ORIENTED_EDGE('',*,*,#2635,.T.);
#3476=ORIENTED_EDGE('',*,*,#2636,.T.);
#3477=ORIENTED_EDGE('',*,*,#2637,.T.);
#3478=ORIENTED_EDGE('',*,*,#2633,.F.);
#3479=ORIENTED_EDGE('',*,*,#2638,.T.);
#3480=ORIENTED_EDGE('',*,*,#2625,.T.);
#3481=ORIENTED_EDGE('',*,*,#2639,.T.);
#3482=ORIENTED_EDGE('',*,*,#2636,.F.);
#3483=ORIENTED_EDGE('',*,*,#2638,.F.);
#3484=ORIENTED_EDGE('',*,*,#2635,.F.);
#3485=ORIENTED_EDGE('',*,*,#2632,.F.);
#3486=ORIENTED_EDGE('',*,*,#2629,.F.);
#3487=ORIENTED_EDGE('',*,*,#2626,.F.);
#3488=ORIENTED_EDGE('',*,*,#2622,.F.);
#3489=ORIENTED_EDGE('',*,*,#2639,.F.);
#3490=ORIENTED_EDGE('',*,*,#2624,.F.);
#3491=ORIENTED_EDGE('',*,*,#2628,.F.);
#3492=ORIENTED_EDGE('',*,*,#2631,.F.);
#3493=ORIENTED_EDGE('',*,*,#2634,.F.);
#3494=ORIENTED_EDGE('',*,*,#2637,.F.);
#3824=CYLINDRICAL_SURFACE('',#4727,0.35);
#3825=CYLINDRICAL_SURFACE('',#4735,0.1954);
#4000=ADVANCED_FACE('',(#746),#514,.T.);
#4001=ADVANCED_FACE('',(#747),#211,.T.);
#4002=ADVANCED_FACE('',(#748),#3824,.T.);
#4003=ADVANCED_FACE('',(#749),#212,.T.);
#4004=ADVANCED_FACE('',(#750,#409),#515,.T.);
#4005=ADVANCED_FACE('',(#751),#213,.T.);
#4006=ADVANCED_FACE('',(#752),#3825,.T.);
#4007=ADVANCED_FACE('',(#753),#214,.T.);
#4008=ADVANCED_FACE('',(#754),#516,.T.);
#4009=ADVANCED_FACE('',(#755),#517,.F.);
#4010=ADVANCED_FACE('',(#756),#518,.F.);
#4011=ADVANCED_FACE('',(#757),#519,.F.);
#4012=ADVANCED_FACE('',(#758),#520,.F.);
#4013=ADVANCED_FACE('',(#759),#521,.F.);
#4014=ADVANCED_FACE('',(#760),#522,.F.);
#4015=ADVANCED_FACE('',(#761),#523,.F.);
#4016=ADVANCED_FACE('',(#762),#524,.F.);
#4102=CLOSED_SHELL('',(#4000,#4001,#4002,#4003,#4004,#4005,#4006,#4007,
#4008));
#4103=CLOSED_SHELL('',(#4009,#4010,#4011,#4012,#4013,#4014,#4015,#4016));
#4722=AXIS2_PLACEMENT_3D('',#6957,#5724,#5725);
#4723=AXIS2_PLACEMENT_3D('',#6958,#5726,#5727);
#4724=AXIS2_PLACEMENT_3D('',#6960,#5728,#5729);
#4725=AXIS2_PLACEMENT_3D('',#6961,#5730,#5731);
#4726=AXIS2_PLACEMENT_3D('',#6963,#5732,#5733);
#4727=AXIS2_PLACEMENT_3D('',#6965,#5735,#5736);
#4728=AXIS2_PLACEMENT_3D('',#6967,#5737,#5738);
#4729=AXIS2_PLACEMENT_3D('',#6969,#5740,#5741);
#4730=AXIS2_PLACEMENT_3D('',#6971,#5742,#5743);
#4731=AXIS2_PLACEMENT_3D('',#6973,#5745,#5746);
#4732=AXIS2_PLACEMENT_3D('',#6975,#5747,#5748);
#4733=AXIS2_PLACEMENT_3D('',#6976,#5749,#5750);
#4734=AXIS2_PLACEMENT_3D('',#6978,#5751,#5752);
#4735=AXIS2_PLACEMENT_3D('',#6980,#5754,#5755);
#4736=AXIS2_PLACEMENT_3D('',#6982,#5756,#5757);
#4737=AXIS2_PLACEMENT_3D('',#6984,#5759,#5760);
#4738=AXIS2_PLACEMENT_3D('',#6986,#5761,#5762);
#4739=AXIS2_PLACEMENT_3D('',#6988,#5764,#5765);
#4740=AXIS2_PLACEMENT_3D('',#6989,#5766,#5767);
#4741=AXIS2_PLACEMENT_3D('',#6998,#5772,#5773);
#4742=AXIS2_PLACEMENT_3D('',#7004,#5777,#5778);
#4743=AXIS2_PLACEMENT_3D('',#7010,#5782,#5783);
#4744=AXIS2_PLACEMENT_3D('',#7016,#5787,#5788);
#4745=AXIS2_PLACEMENT_3D('',#7022,#5792,#5793);
#4746=AXIS2_PLACEMENT_3D('',#7025,#5796,#5797);
#4747=AXIS2_PLACEMENT_3D('',#7026,#5798,#5799);
#5724=DIRECTION('axis',(0.,0.,1.));
#5725=DIRECTION('refdir',(1.,0.,0.));
#5726=DIRECTION('center_axis',(0.,1.,0.));
#5727=DIRECTION('ref_axis',(0.,0.,1.));
#5728=DIRECTION('center_axis',(0.,-1.,0.));
#5729=DIRECTION('ref_axis',(1.,0.,0.));
#5730=DIRECTION('center_axis',(0.,-1.,0.));
#5731=DIRECTION('ref_axis',(1.,0.,0.));
#5732=DIRECTION('center_axis',(0.,-1.,0.));
#5733=DIRECTION('ref_axis',(1.,0.,0.));
#5734=DIRECTION('',(0.707106781186547,0.707106781186548,8.65956056235493E-17));
#5735=DIRECTION('center_axis',(0.,-1.,0.));
#5736=DIRECTION('ref_axis',(1.,0.,0.));
#5737=DIRECTION('center_axis',(0.,-1.,0.));
#5738=DIRECTION('ref_axis',(1.,0.,0.));
#5739=DIRECTION('',(0.,1.,0.));
#5740=DIRECTION('center_axis',(0.,1.,0.));
#5741=DIRECTION('ref_axis',(1.,0.,0.));
#5742=DIRECTION('center_axis',(0.,-1.,0.));
#5743=DIRECTION('ref_axis',(1.,0.,0.));
#5744=DIRECTION('',(-0.707106781186547,0.707106781186548,-8.65956056235493E-17));
#5745=DIRECTION('center_axis',(0.,-1.,0.));
#5746=DIRECTION('ref_axis',(0.,0.,-1.));
#5747=DIRECTION('center_axis',(0.,-1.,0.));
#5748=DIRECTION('ref_axis',(1.,0.,0.));
#5749=DIRECTION('center_axis',(0.,1.,0.));
#5750=DIRECTION('ref_axis',(1.,0.,0.));
#5751=DIRECTION('center_axis',(0.,1.,0.));
#5752=DIRECTION('ref_axis',(1.,0.,0.));
#5753=DIRECTION('',(-0.447213595499958,0.894427190999916,-5.47678698264203E-17));
#5754=DIRECTION('center_axis',(0.,-1.,0.));
#5755=DIRECTION('ref_axis',(1.,0.,0.));
#5756=DIRECTION('center_axis',(0.,1.,0.));
#5757=DIRECTION('ref_axis',(1.,0.,0.));
#5758=DIRECTION('',(0.,1.,0.));
#5759=DIRECTION('center_axis',(0.,1.,0.));
#5760=DIRECTION('ref_axis',(1.,0.,0.));
#5761=DIRECTION('center_axis',(0.,-1.,0.));
#5762=DIRECTION('ref_axis',(1.,0.,0.));
#5763=DIRECTION('',(-0.707106781186547,0.707106781186548,-8.65956056235493E-17));
#5764=DIRECTION('center_axis',(0.,-1.,0.));
#5765=DIRECTION('ref_axis',(0.,0.,-1.));
#5766=DIRECTION('center_axis',(0.866025403784439,0.,-0.5));
#5767=DIRECTION('ref_axis',(0.5,0.,0.866025403784439));
#5768=DIRECTION('',(-0.5,0.,-0.866025403784439));
#5769=DIRECTION('',(0.,-1.,0.));
#5770=DIRECTION('',(0.5,0.,0.866025403784439));
#5771=DIRECTION('',(0.,-1.,0.));
#5772=DIRECTION('center_axis',(1.60246890531964E-16,0.,-1.));
#5773=DIRECTION('ref_axis',(1.,0.,1.60246890531964E-16));
#5774=DIRECTION('',(-1.,0.,-1.60246890531964E-16));
#5775=DIRECTION('',(0.,-1.,0.));
#5776=DIRECTION('',(1.,0.,1.60246890531964E-16));
#5777=DIRECTION('center_axis',(-0.866025403784439,0.,-0.5));
#5778=DIRECTION('ref_axis',(0.5,0.,-0.866025403784439));
#5779=DIRECTION('',(-0.5,0.,0.866025403784439));
#5780=DIRECTION('',(0.,-1.,0.));
#5781=DIRECTION('',(0.5,0.,-0.866025403784439));
#5782=DIRECTION('center_axis',(-0.866025403784439,0.,0.5));
#5783=DIRECTION('ref_axis',(-0.5,0.,-0.866025403784439));
#5784=DIRECTION('',(0.5,0.,0.866025403784439));
#5785=DIRECTION('',(0.,-1.,0.));
#5786=DIRECTION('',(-0.5,0.,-0.866025403784439));
#5787=DIRECTION('center_axis',(-1.60246890531964E-16,0.,1.));
#5788=DIRECTION('ref_axis',(-1.,0.,-1.60246890531964E-16));
#5789=DIRECTION('',(1.,0.,1.60246890531964E-16));
#5790=DIRECTION('',(0.,-1.,0.));
#5791=DIRECTION('',(-1.,0.,-1.60246890531964E-16));
#5792=DIRECTION('center_axis',(0.866025403784439,0.,0.5));
#5793=DIRECTION('ref_axis',(-0.5,0.,0.866025403784439));
#5794=DIRECTION('',(0.5,0.,-0.866025403784439));
#5795=DIRECTION('',(-0.5,0.,0.866025403784439));
#5796=DIRECTION('center_axis',(0.,1.,0.));
#5797=DIRECTION('ref_axis',(1.,0.,0.));
#5798=DIRECTION('center_axis',(0.,-1.,0.));
#5799=DIRECTION('ref_axis',(0.,0.,-1.));
#6957=CARTESIAN_POINT('',(0.,0.,0.));
#6958=CARTESIAN_POINT('Origin',(0.3,0.4,0.));
#6959=CARTESIAN_POINT('',(-0.3,0.4,-3.67394039744206E-17));
#6960=CARTESIAN_POINT('Origin',(0.,0.4,0.));
#6961=CARTESIAN_POINT('Origin',(0.,0.375,0.));
#6962=CARTESIAN_POINT('',(-0.35,0.35,-4.28626379701573E-17));
#6963=CARTESIAN_POINT('Origin',(0.,0.35,0.));
#6964=CARTESIAN_POINT('',(-0.325,0.375,-3.9801020972289E-17));
#6965=CARTESIAN_POINT('Origin',(0.,0.19,0.));
#6966=CARTESIAN_POINT('',(-0.35,0.03,-4.28626379701574E-17));
#6967=CARTESIAN_POINT('Origin',(0.,0.03,0.));
#6968=CARTESIAN_POINT('',(-0.35,0.19,-4.28626379701574E-17));
#6969=CARTESIAN_POINT('Origin',(0.,0.0149999999999999,0.));
#6970=CARTESIAN_POINT('',(-0.32,-3.29597460435593E-17,-3.91886975727153E-17));
#6971=CARTESIAN_POINT('Origin',(0.,0.,0.));
#6972=CARTESIAN_POINT('',(-0.335,0.0149999999999999,-4.10256677714363E-17));
#6973=CARTESIAN_POINT('Origin',(0.22,0.,0.));
#6974=CARTESIAN_POINT('',(-0.22,-6.93889390390723E-18,-2.69422295812418E-17));
#6975=CARTESIAN_POINT('Origin',(0.,0.,0.));
#6976=CARTESIAN_POINT('Origin',(0.,-0.02,0.));
#6977=CARTESIAN_POINT('',(-0.1954,-0.0492,2.39295984553393E-17));
#6978=CARTESIAN_POINT('Origin',(0.,-0.0492,0.));
#6979=CARTESIAN_POINT('',(-0.21,-0.02,-2.57175827820944E-17));
#6980=CARTESIAN_POINT('Origin',(0.,-0.8,0.));
#6981=CARTESIAN_POINT('',(-0.1954,-1.5646,2.39295984553393E-17));
#6982=CARTESIAN_POINT('Origin',(0.,-1.5646,0.));
#6983=CARTESIAN_POINT('',(-0.1954,-0.8,-2.39295984553393E-17));
#6984=CARTESIAN_POINT('Origin',(0.,-1.58,0.));
#6985=CARTESIAN_POINT('',(-0.16,-1.6,-1.95943487863577E-17));
#6986=CARTESIAN_POINT('Origin',(0.,-1.6,0.));
#6987=CARTESIAN_POINT('',(-0.18,-1.58,-2.20436423846524E-17));
#6988=CARTESIAN_POINT('Origin',(0.,-1.6,0.));
#6989=CARTESIAN_POINT('Origin',(0.0866025403784439,-0.4,-0.15));
#6990=CARTESIAN_POINT('',(0.173205080756888,-0.4,0.));
#6991=CARTESIAN_POINT('',(0.0866025403784439,-0.4,-0.15));
#6992=CARTESIAN_POINT('',(0.173205080756888,-0.4,0.));
#6993=CARTESIAN_POINT('',(0.0866025403784439,-0.64,-0.15));
#6994=CARTESIAN_POINT('',(0.0866025403784439,-0.4,-0.15));
#6995=CARTESIAN_POINT('',(0.173205080756888,-0.64,0.));
#6996=CARTESIAN_POINT('',(0.173205080756888,-0.64,0.));
#6997=CARTESIAN_POINT('',(0.173205080756888,-0.4,0.));
#6998=CARTESIAN_POINT('Origin',(-0.0866025403784438,-0.4,-0.15));
#6999=CARTESIAN_POINT('',(-0.0866025403784438,-0.4,-0.15));
#7000=CARTESIAN_POINT('',(0.0866025403784439,-0.4,-0.15));
#7001=CARTESIAN_POINT('',(-0.0866025403784438,-0.64,-0.15));
#7002=CARTESIAN_POINT('',(-0.0866025403784438,-0.4,-0.15));
#7003=CARTESIAN_POINT('',(0.0866025403784439,-0.64,-0.15));
#7004=CARTESIAN_POINT('Origin',(-0.173205080756888,-0.4,-2.77555756156289E-17));
#7005=CARTESIAN_POINT('',(-0.173205080756888,-0.4,-2.12115047744981E-17));
#7006=CARTESIAN_POINT('',(-0.0866025403784438,-0.4,-0.15));
#7007=CARTESIAN_POINT('',(-0.173205080756888,-0.64,-2.77555756156289E-17));
#7008=CARTESIAN_POINT('',(-0.173205080756888,-0.4,-2.12115047744981E-17));
#7009=CARTESIAN_POINT('',(-0.0866025403784438,-0.64,-0.15));
#7010=CARTESIAN_POINT('Origin',(-0.0866025403784439,-0.4,0.15));
#7011=CARTESIAN_POINT('',(-0.0866025403784439,-0.4,0.15));
#7012=CARTESIAN_POINT('',(-0.173205080756888,-0.4,-2.12115047744981E-17));
#7013=CARTESIAN_POINT('',(-0.0866025403784439,-0.64,0.15));
#7014=CARTESIAN_POINT('',(-0.0866025403784439,-0.4,0.15));
#7015=CARTESIAN_POINT('',(-0.173205080756888,-0.64,-2.12115047744981E-17));
#7016=CARTESIAN_POINT('Origin',(0.0866025403784439,-0.4,0.15));
#7017=CARTESIAN_POINT('',(0.0866025403784439,-0.4,0.15));
#7018=CARTESIAN_POINT('',(-0.0866025403784439,-0.4,0.15));
#7019=CARTESIAN_POINT('',(0.0866025403784439,-0.64,0.15));
#7020=CARTESIAN_POINT('',(0.0866025403784439,-0.4,0.15));
#7021=CARTESIAN_POINT('',(-0.0866025403784439,-0.64,0.15));
#7022=CARTESIAN_POINT('Origin',(0.173205080756888,-0.4,0.));
#7023=CARTESIAN_POINT('',(0.0866025403784439,-0.4,0.15));
#7024=CARTESIAN_POINT('',(0.0866025403784439,-0.64,0.15));
#7025=CARTESIAN_POINT('Origin',(0.,-0.4,-2.77555756156289E-17));
#7026=CARTESIAN_POINT('Origin',(0.,-0.64,-2.77555756156289E-17));
#7387=UNCERTAINTY_MEASURE_WITH_UNIT(LENGTH_MEASURE(0.001),#7426,
'DISTANCE_ACCURACY_VALUE',
'Maximum model space distance between geometric entities at asserted c
onnectivities');
#7395=UNCERTAINTY_MEASURE_WITH_UNIT(LENGTH_MEASURE(0.001),#7426,
'DISTANCE_ACCURACY_VALUE',
'Maximum model space distance between geometric entities at asserted c
onnectivities');
#7417=(
GEOMETRIC_REPRESENTATION_CONTEXT(3)
GLOBAL_UNCERTAINTY_ASSIGNED_CONTEXT((#7387))
GLOBAL_UNIT_ASSIGNED_CONTEXT((#7426,#7428,#7429))
REPRESENTATION_CONTEXT('','3D')
);
#7425=(
GEOMETRIC_REPRESENTATION_CONTEXT(3)
GLOBAL_UNCERTAINTY_ASSIGNED_CONTEXT((#7395))
GLOBAL_UNIT_ASSIGNED_CONTEXT((#7426,#7428,#7429))
REPRESENTATION_CONTEXT('','3D')
);
#7426=(
LENGTH_UNIT()
NAMED_UNIT(*)
SI_UNIT(.CENTI.,.METRE.)
);
#7428=(
NAMED_UNIT(*)
PLANE_ANGLE_UNIT()
SI_UNIT($,.RADIAN.)
);
#7429=(
NAMED_UNIT(*)
SI_UNIT($,.STERADIAN.)
SOLID_ANGLE_UNIT()
);
#7451=SHAPE_DEFINITION_REPRESENTATION(#7480,#7554);
#7480=PRODUCT_DEFINITION_SHAPE('',$,#7584);
#7554=SHAPE_REPRESENTATION('',(#4722),#7417);
#7562=PRODUCT_DEFINITION_CONTEXT('part definition',#7651,'design');
#7584=PRODUCT_DEFINITION('Cap Screw - M4x16','Cap Screw - M4x16',#7613,
#7562);
#7613=PRODUCT_DEFINITION_FORMATION('',$,#7674);
#7651=APPLICATION_CONTEXT(
'Core Data for Automotive Mechanical Design Process');
#7652=PRODUCT_CONTEXT('part definition',#7651,'mechanical');
#7674=PRODUCT('Cap Screw - M4x16','Cap Screw - M4x16',
'Cap Screw - M4x16',(#7652));
#7745=COLOUR_RGB('Black',0.12,0.14,0.17);
#7746=FILL_AREA_STYLE_COLOUR('',#7745);
#7747=FILL_AREA_STYLE('',(#7746));
#7748=SURFACE_STYLE_FILL_AREA(#7747);
#7749=SURFACE_SIDE_STYLE('',(#7748));
#7750=SURFACE_STYLE_USAGE(.BOTH.,#7749);
#7751=PRESENTATION_STYLE_ASSIGNMENT((#7750));
ENDSEC;
END-ISO-10303-21;
